ISO-10303-21;
HEADER;
/* Generated by software containing ST-Developer
 * from STEP Tools, Inc. (www.steptools.com) 
 */
/* OPTION: using custom renumber hook */

FILE_DESCRIPTION(
/* description */ ('STEP AP242 Edition 2', 'CAx-IF Rec.Pracs.---Representation and Presentation of Product Manufa
cturing Information (PMI)---4.0---2014-10-13', 'CAx-IF Rec.Pracs.---3D Tessellated Geometry---0.4---2014-09-14', '2;1', 'CAx-IF Rec.Pracs.---User Defined Attributes---1.5---2016-08-15'),
/* implementation_level */ '2;1');

FILE_NAME(
/* name */ 'Floating_ring_guide.step',
/* time_stamp */ '2026-10-08T12:15:07Z',
/* author */ (''),
/* organization */ (''),
/* preprocessor_version */ 'ST-DEVELOPER v20',
/* originating_system */ 'ONSHAPE BY PTC INC, 1.221',
/* authorisation */ '  ');

FILE_SCHEMA (('AP242_MANAGED_MODEL_BASED_3D_ENGINEERING_MIM_LF { 1 0 10303 442 3 1 4 }'));
ENDSEC;

DATA;
#10=VERTEX_LOOP('',#7790);
#11=VERTEX_LOOP('',#7792);
#23=CONICAL_SURFACE('',#14271,0.0012192,1.02974425867665);
#24=CONICAL_SURFACE('',#14272,0.0012192,1.02974425867665);
#60=COLOUR_RGB('', 0.66274510, 0.83137255, 0.94901961);
#208=SHAPE_REPRESENTATION_RELATIONSHIP('','',#13782,#235);
#235=ADVANCED_BREP_SHAPE_REPRESENTATION('',(#13726),#45472);
#585=CIRCLE('',#14263,0.004);
#586=CIRCLE('',#14264,0.0012192);
#587=CIRCLE('',#14266,0.004);
#588=CIRCLE('',#14267,0.0012192);
#589=CIRCLE('',#14270,0.0012192);
#590=CIRCLE('',#14273,0.0012192);
#1271=PLANE('',#14262);
#1272=PLANE('',#14265);
#1616=CYLINDRICAL_SURFACE('',#14268,0.004);
#1617=CYLINDRICAL_SURFACE('',#14269,0.0012192);
#1618=CYLINDRICAL_SURFACE('',#14274,0.0012192);
#2876=ORIENTED_EDGE('',*,*,#6085,.F.);
#2877=ORIENTED_EDGE('',*,*,#6086,.T.);
#2878=ORIENTED_EDGE('',*,*,#6087,.T.);
#2879=ORIENTED_EDGE('',*,*,#6088,.F.);
#2880=ORIENTED_EDGE('',*,*,#6085,.T.);
#2881=ORIENTED_EDGE('',*,*,#6087,.F.);
#2882=ORIENTED_EDGE('',*,*,#6086,.F.);
#2883=ORIENTED_EDGE('',*,*,#6089,.F.);
#2884=ORIENTED_EDGE('',*,*,#6089,.T.);
#2885=ORIENTED_EDGE('',*,*,#6090,.T.);
#2886=ORIENTED_EDGE('',*,*,#6088,.T.);
#2887=ORIENTED_EDGE('',*,*,#6090,.F.);
#6085=EDGE_CURVE('',#7785,#7785,#585,.T.);
#6086=EDGE_CURVE('',#7786,#7786,#586,.T.);
#6087=EDGE_CURVE('',#7787,#7787,#587,.T.);
#6088=EDGE_CURVE('',#7788,#7788,#588,.T.);
#6089=EDGE_CURVE('',#7789,#7789,#589,.T.);
#6090=EDGE_CURVE('',#7791,#7791,#590,.T.);
#7785=VERTEX_POINT('',#31667);
#7786=VERTEX_POINT('',#31669);
#7787=VERTEX_POINT('',#31672);
#7788=VERTEX_POINT('',#31674);
#7789=VERTEX_POINT('',#31678);
#7790=VERTEX_POINT('',#31680);
#7791=VERTEX_POINT('',#31683);
#7792=VERTEX_POINT('',#31684);
#10777=EDGE_LOOP('',(#2876));
#10778=EDGE_LOOP('',(#2877));
#10779=EDGE_LOOP('',(#2878));
#10780=EDGE_LOOP('',(#2879));
#10781=EDGE_LOOP('',(#2880));
#10782=EDGE_LOOP('',(#2881));
#10783=EDGE_LOOP('',(#2882));
#10784=EDGE_LOOP('',(#2883));
#10785=EDGE_LOOP('',(#2884));
#10786=EDGE_LOOP('',(#2885));
#10787=EDGE_LOOP('',(#2886));
#10788=EDGE_LOOP('',(#2887));
#11892=FACE_BOUND('',#10777,.T.);
#11893=FACE_BOUND('',#10778,.T.);
#11894=FACE_BOUND('',#10779,.T.);
#11895=FACE_BOUND('',#10780,.T.);
#11896=FACE_BOUND('',#10781,.T.);
#11897=FACE_BOUND('',#10782,.T.);
#11898=FACE_BOUND('',#10783,.T.);
#11899=FACE_BOUND('',#10784,.T.);
#11900=FACE_BOUND('',#10785,.T.);
#11901=FACE_BOUND('',#10,.T.);
#11902=FACE_BOUND('',#10786,.T.);
#11903=FACE_BOUND('',#11,.T.);
#11904=FACE_BOUND('',#10787,.T.);
#11905=FACE_BOUND('',#10788,.T.);
#12936=ADVANCED_FACE('',(#11892,#11893),#1271,.F.);
#12937=ADVANCED_FACE('',(#11894,#11895),#1272,.T.);
#12938=ADVANCED_FACE('',(#11896,#11897),#1616,.T.);
#12939=ADVANCED_FACE('',(#11898,#11899),#1617,.F.);
#12940=ADVANCED_FACE('',(#11900,#11901),#23,.F.);
#12941=ADVANCED_FACE('',(#11902,#11903),#24,.F.);
#12942=ADVANCED_FACE('',(#11904,#11905),#1618,.F.);
#13509=CLOSED_SHELL('',(#12936,#12937,#12938,#12939,#12940,#12941,#12942));
#13536=STYLED_ITEM('',(#13563),#13726);
#13563=PRESENTATION_STYLE_ASSIGNMENT((#13590));
#13590=SURFACE_STYLE_USAGE(.BOTH.,#13617);
#13617=SURFACE_SIDE_STYLE('',(#13644));
#13644=SURFACE_STYLE_FILL_AREA(#13671);
#13671=FILL_AREA_STYLE('',(#13698));
#13698=FILL_AREA_STYLE_COLOUR('',#60);
#13726=MANIFOLD_SOLID_BREP('Floating_ring_guide',#13509);
#13754=SHAPE_DEFINITION_REPRESENTATION(#45539,#13782);
#13782=SHAPE_REPRESENTATION('Floating_ring_guide',(#13802),#45472);
#13802=AXIS2_PLACEMENT_3D('',#19109,#15295,#15296);
#14262=AXIS2_PLACEMENT_3D('',#31665,#16334,#16335);
#14263=AXIS2_PLACEMENT_3D('',#31666,#16336,#16337);
#14264=AXIS2_PLACEMENT_3D('',#31668,#16338,#16339);
#14265=AXIS2_PLACEMENT_3D('',#31670,#16340,#16341);
#14266=AXIS2_PLACEMENT_3D('',#31671,#16342,#16343);
#14267=AXIS2_PLACEMENT_3D('',#31673,#16344,#16345);
#14268=AXIS2_PLACEMENT_3D('',#31675,#16346,#16347);
#14269=AXIS2_PLACEMENT_3D('',#31676,#16348,#16349);
#14270=AXIS2_PLACEMENT_3D('',#31677,#16350,#16351);
#14271=AXIS2_PLACEMENT_3D('',#31679,#16352,#16353);
#14272=AXIS2_PLACEMENT_3D('',#31681,#16354,#16355);
#14273=AXIS2_PLACEMENT_3D('',#31682,#16356,#16357);
#14274=AXIS2_PLACEMENT_3D('',#31685,#16358,#16359);
#15295=DIRECTION('',(0.,0.,1.));
#15296=DIRECTION('',(1.,0.,0.));
#16334=DIRECTION('',(0.,0.,-1.));
#16335=DIRECTION('',(-1.,0.,0.));
#16336=DIRECTION('',(0.,0.,-1.));
#16337=DIRECTION('',(-1.,0.,0.));
#16338=DIRECTION('',(0.,0.,-1.));
#16339=DIRECTION('',(-1.,0.,0.));
#16340=DIRECTION('',(0.,0.,-1.));
#16341=DIRECTION('',(-1.,0.,0.));
#16342=DIRECTION('',(0.,0.,-1.));
#16343=DIRECTION('',(-1.,0.,0.));
#16344=DIRECTION('',(0.,0.,-1.));
#16345=DIRECTION('',(-1.,0.,0.));
#16346=DIRECTION('',(0.,0.,1.));
#16347=DIRECTION('',(1.,0.,0.));
#16348=DIRECTION('',(0.,0.,-1.));
#16349=DIRECTION('',(-1.,0.,0.));
#16350=DIRECTION('',(0.,0.,1.));
#16351=DIRECTION('',(1.,0.,0.));
#16352=DIRECTION('',(0.,0.,1.));
#16353=DIRECTION('',(1.,0.,0.));
#16354=DIRECTION('',(0.,0.,-1.));
#16355=DIRECTION('',(-1.,0.,0.));
#16356=DIRECTION('',(0.,0.,-1.));
#16357=DIRECTION('',(-1.,0.,0.));
#16358=DIRECTION('',(0.,0.,-1.));
#16359=DIRECTION('',(-1.,0.,0.));
#19109=CARTESIAN_POINT('',(0.,0.,0.));
#31665=CARTESIAN_POINT('',(0.,0.03,0.1));
#31666=CARTESIAN_POINT('',(0.,0.03,0.1));
#31667=CARTESIAN_POINT('',(-0.004,0.03,0.1));
#31668=CARTESIAN_POINT('',(0.,0.03,0.1));
#31669=CARTESIAN_POINT('',(-0.0012192,0.03,0.1));
#31670=CARTESIAN_POINT('',(0.,0.03,0.067));
#31671=CARTESIAN_POINT('',(0.,0.03,0.067));
#31672=CARTESIAN_POINT('',(-0.004,0.03,0.067));
#31673=CARTESIAN_POINT('',(0.,0.03,0.067));
#31674=CARTESIAN_POINT('',(-0.0012192,0.03,0.067));
#31675=CARTESIAN_POINT('',(0.,0.03,0.067));
#31676=CARTESIAN_POINT('',(0.,0.03,0.064));
#31677=CARTESIAN_POINT('',(0.,0.03,0.0936825692667184));
#31678=CARTESIAN_POINT('',(0.0012192,0.03,0.0936825692667184));
#31679=CARTESIAN_POINT('',(0.,0.03,0.0936825692667184));
#31680=CARTESIAN_POINT('',(-2.60208521396521E-18,0.03,0.09295));
#31681=CARTESIAN_POINT('',(0.,0.03,0.0733174307332816));
#31682=CARTESIAN_POINT('',(0.,0.03,0.0733174307332816));
#31683=CARTESIAN_POINT('',(-0.0012192,0.03,0.0733174307332816));
#31684=CARTESIAN_POINT('',(-2.60208521396521E-18,0.03,0.07405));
#31685=CARTESIAN_POINT('',(0.,0.03,0.064));
#45463=MECHANICAL_DESIGN_GEOMETRIC_PRESENTATION_REPRESENTATION('',(#13536),#45464);
#45464=(
GEOMETRIC_REPRESENTATION_CONTEXT(3)
GLOBAL_UNCERTAINTY_ASSIGNED_CONTEXT((#45492))
GLOBAL_UNIT_ASSIGNED_CONTEXT((#45522,#45521,#45520))
REPRESENTATION_CONTEXT('MAS-690','TOP_LEVEL_ASSEMBLY_PART')
);
#45472=(
GEOMETRIC_REPRESENTATION_CONTEXT(3)
GLOBAL_UNCERTAINTY_ASSIGNED_CONTEXT((#45500))
GLOBAL_UNIT_ASSIGNED_CONTEXT((#45522,#45521,#45520))
REPRESENTATION_CONTEXT('Floating_ring_guide','COMPONENT_PART')
);
#45492=UNCERTAINTY_MEASURE_WITH_UNIT(LENGTH_MEASURE(1.E-8),#45522,
'DISTANCE_ACCURACY_VALUE','Maximum Tolerance applied to model');
#45500=UNCERTAINTY_MEASURE_WITH_UNIT(LENGTH_MEASURE(1.E-6),#45522,
'DISTANCE_ACCURACY_VALUE','Maximum Tolerance applied to model');
#45520=(
NAMED_UNIT(*)
SI_UNIT($,.STERADIAN.)
SOLID_ANGLE_UNIT()
);
#45521=(
NAMED_UNIT(*)
PLANE_ANGLE_UNIT()
SI_UNIT($,.RADIAN.)
);
#45522=(
LENGTH_UNIT()
NAMED_UNIT(*)
SI_UNIT($,.METRE.)
);
#45539=PRODUCT_DEFINITION_SHAPE('','',#45593);
#45593=PRODUCT_DEFINITION('','',#45649,#45621);
#45621=PRODUCT_DEFINITION_CONTEXT('',#45782,'design');
#45649=PRODUCT_DEFINITION_FORMATION_WITH_SPECIFIED_SOURCE('','',#45705,
 .NOT_KNOWN.);
#45705=PRODUCT('Floating_ring_guide','Floating_ring_guide',
'Floating_ring_guide',(#45761));
#45761=PRODUCT_CONTEXT('',#45782,'mechanical');
#45782=APPLICATION_CONTEXT('managed model based 3d engineering');
ENDSEC;
END-ISO-10303-21;
